ISO-10303-21;
HEADER;
/* Generated by software containing ST-Developer
 * from STEP Tools, Inc. (www.steptools.com) 
 */

FILE_DESCRIPTION(
/* description */ ('Hand-operated arbor press'),
/* implementation_level */ '2;1');

FILE_NAME(
/* name */ 'Cap Screw - M4x16.step',
/* time_stamp */ '2026-10-28T03:25:25-07:00',
/* author */ (''),
/* organization */ (''),
/* preprocessor_version */ 'ST-DEVELOPER v20.2',
/* originating_system */ 'Autodesk Translation Framework v15.17.0.0',
/* authorisation */ '');

FILE_SCHEMA (('AUTOMOTIVE_DESIGN { 1 0 10303 214 3 1 1 }'));
ENDSEC;

DATA;
#10=MECHANICAL_DESIGN_GEOMETRIC_PRESENTATION_REPRESENTATION('',(#633),#32751);
#476=ORIENTED_CLOSED_SHELL('',*,#12534,.F.);
#494=CONICAL_SURFACE('',#14054,0.325,0.785398163397448);
#495=CONICAL_SURFACE('',#14058,0.335,0.785398163397448);
#496=CONICAL_SURFACE('',#14062,0.21,0.463647609000806);
#497=CONICAL_SURFACE('',#14066,0.18,0.785398163397448);
#501=BREP_WITH_VOIDS('Body1',#12533,(#476));
#542=SHAPE_REPRESENTATION_RELATIONSHIP('SRR','None',#32974,#584);
#584=ADVANCED_BREP_SHAPE_REPRESENTATION('',(#501),#32748);
#633=STYLED_ITEM('',(#33249),#501);
#846=FACE_BOUND('',#2805,.T.);
#1280=PLANE('',#14052);
#1281=PLANE('',#14060);
#1282=PLANE('',#14068);
#1283=PLANE('',#14069);
#1284=PLANE('',#14070);
#1285=PLANE('',#14071);
#1286=PLANE('',#14072);
#1287=PLANE('',#14073);
#1288=PLANE('',#14074);
#1289=PLANE('',#14075);
#1290=PLANE('',#14076);
#1953=FACE_OUTER_BOUND('',#2800,.T.);
#1954=FACE_OUTER_BOUND('',#2801,.T.);
#1955=FACE_OUTER_BOUND('',#2802,.T.);
#1956=FACE_OUTER_BOUND('',#2803,.T.);
#1957=FACE_OUTER_BOUND('',#2804,.T.);
#1958=FACE_OUTER_BOUND('',#2806,.T.);
#1959=FACE_OUTER_BOUND('',#2807,.T.);
#1960=FACE_OUTER_BOUND('',#2808,.T.);
#1961=FACE_OUTER_BOUND('',#2809,.T.);
#1962=FACE_OUTER_BOUND('',#2810,.T.);
#1963=FACE_OUTER_BOUND('',#2811,.T.);
#1964=FACE_OUTER_BOUND('',#2812,.T.);
#1965=FACE_OUTER_BOUND('',#2813,.T.);
#1966=FACE_OUTER_BOUND('',#2814,.T.);
#1967=FACE_OUTER_BOUND('',#2815,.T.);
#1968=FACE_OUTER_BOUND('',#2816,.T.);
#1969=FACE_OUTER_BOUND('',#2817,.T.);
#2800=EDGE_LOOP('',(#11566));
#2801=EDGE_LOOP('',(#11567,#11568,#11569,#11570));
#2802=EDGE_LOOP('',(#11571,#11572,#11573,#11574));
#2803=EDGE_LOOP('',(#11575,#11576,#11577,#11578));
#2804=EDGE_LOOP('',(#11579));
#2805=EDGE_LOOP('',(#11580));
#2806=EDGE_LOOP('',(#11581,#11582,#11583,#11584));
#2807=EDGE_LOOP('',(#11585,#11586,#11587,#11588));
#2808=EDGE_LOOP('',(#11589,#11590,#11591,#11592));
#2809=EDGE_LOOP('',(#11593));
#2810=EDGE_LOOP('',(#11594,#11595,#11596,#11597));
#2811=EDGE_LOOP('',(#11598,#11599,#11600,#11601));
#2812=EDGE_LOOP('',(#11602,#11603,#11604,#11605));
#2813=EDGE_LOOP('',(#11606,#11607,#11608,#11609));
#2814=EDGE_LOOP('',(#11610,#11611,#11612,#11613));
#2815=EDGE_LOOP('',(#11614,#11615,#11616,#11617));
#2816=EDGE_LOOP('',(#11618,#11619,#11620,#11621,#11622,#11623));
#2817=EDGE_LOOP('',(#11624,#11625,#11626,#11627,#11628,#11629));
#3969=LINE('',#32507,#5140);
#3970=LINE('',#32511,#5141);
#3971=LINE('',#32515,#5142);
#3972=LINE('',#32522,#5143);
#3973=LINE('',#32526,#5144);
#3974=LINE('',#32530,#5145);
#3975=LINE('',#32535,#5146);
#3976=LINE('',#32537,#5147);
#3977=LINE('',#32539,#5148);
#3978=LINE('',#32540,#5149);
#3979=LINE('',#32543,#5150);
#3980=LINE('',#32545,#5151);
#3981=LINE('',#32546,#5152);
#3982=LINE('',#32549,#5153);
#3983=LINE('',#32551,#5154);
#3984=LINE('',#32552,#5155);
#3985=LINE('',#32555,#5156);
#3986=LINE('',#32557,#5157);
#3987=LINE('',#32558,#5158);
#3988=LINE('',#32561,#5159);
#3989=LINE('',#32563,#5160);
#3990=LINE('',#32564,#5161);
#3991=LINE('',#32566,#5162);
#3992=LINE('',#32567,#5163);
#5140=VECTOR('',#17414,0.325);
#5141=VECTOR('',#17419,0.35);
#5142=VECTOR('',#17424,0.335);
#5143=VECTOR('',#17433,0.21);
#5144=VECTOR('',#17438,0.2);
#5145=VECTOR('',#17443,0.18);
#5146=VECTOR('',#17448,1.);
#5147=VECTOR('',#17449,1.);
#5148=VECTOR('',#17450,1.);
#5149=VECTOR('',#17451,1.);
#5150=VECTOR('',#17454,1.);
#5151=VECTOR('',#17455,1.);
#5152=VECTOR('',#17456,1.);
#5153=VECTOR('',#17459,1.);
#5154=VECTOR('',#17460,1.);
#5155=VECTOR('',#17461,1.);
#5156=VECTOR('',#17464,1.);
#5157=VECTOR('',#17465,1.);
#5158=VECTOR('',#17466,1.);
#5159=VECTOR('',#17469,1.);
#5160=VECTOR('',#17470,1.);
#5161=VECTOR('',#17471,1.);
#5162=VECTOR('',#17474,1.);
#5163=VECTOR('',#17475,1.);
#5544=CIRCLE('',#14053,0.3);
#5545=CIRCLE('',#14055,0.35);
#5546=CIRCLE('',#14057,0.35);
#5547=CIRCLE('',#14059,0.32);
#5548=CIRCLE('',#14061,0.22);
#5549=CIRCLE('',#14063,0.1954);
#5550=CIRCLE('',#14065,0.1954);
#5551=CIRCLE('',#14067,0.16);
#6641=VERTEX_POINT('',#32502);
#6642=VERTEX_POINT('',#32505);
#6643=VERTEX_POINT('',#32509);
#6644=VERTEX_POINT('',#32513);
#6645=VERTEX_POINT('',#32517);
#6646=VERTEX_POINT('',#32520);
#6647=VERTEX_POINT('',#32524);
#6648=VERTEX_POINT('',#32528);
#6649=VERTEX_POINT('',#32533);
#6650=VERTEX_POINT('',#32534);
#6651=VERTEX_POINT('',#32536);
#6652=VERTEX_POINT('',#32538);
#6653=VERTEX_POINT('',#32542);
#6654=VERTEX_POINT('',#32544);
#6655=VERTEX_POINT('',#32548);
#6656=VERTEX_POINT('',#32550);
#6657=VERTEX_POINT('',#32554);
#6658=VERTEX_POINT('',#32556);
#6659=VERTEX_POINT('',#32560);
#6660=VERTEX_POINT('',#32562);
#8286=EDGE_CURVE('',#6641,#6641,#5544,.T.);
#8287=EDGE_CURVE('',#6642,#6642,#5545,.T.);
#8288=EDGE_CURVE('',#6642,#6641,#3969,.T.);
#8289=EDGE_CURVE('',#6643,#6643,#5546,.T.);
#8290=EDGE_CURVE('',#6643,#6642,#3970,.T.);
#8291=EDGE_CURVE('',#6644,#6644,#5547,.T.);
#8292=EDGE_CURVE('',#6644,#6643,#3971,.T.);
#8293=EDGE_CURVE('',#6645,#6645,#5548,.T.);
#8294=EDGE_CURVE('',#6646,#6646,#5549,.F.);
#8295=EDGE_CURVE('',#6646,#6645,#3972,.T.);
#8296=EDGE_CURVE('',#6647,#6647,#5550,.F.);
#8297=EDGE_CURVE('',#6647,#6646,#3973,.T.);
#8298=EDGE_CURVE('',#6648,#6648,#5551,.T.);
#8299=EDGE_CURVE('',#6648,#6647,#3974,.T.);
#8300=EDGE_CURVE('',#6649,#6650,#3975,.T.);
#8301=EDGE_CURVE('',#6650,#6651,#3976,.T.);
#8302=EDGE_CURVE('',#6651,#6652,#3977,.T.);
#8303=EDGE_CURVE('',#6649,#6652,#3978,.T.);
#8304=EDGE_CURVE('',#6650,#6653,#3979,.T.);
#8305=EDGE_CURVE('',#6653,#6654,#3980,.T.);
#8306=EDGE_CURVE('',#6654,#6651,#3981,.T.);
#8307=EDGE_CURVE('',#6653,#6655,#3982,.T.);
#8308=EDGE_CURVE('',#6655,#6656,#3983,.T.);
#8309=EDGE_CURVE('',#6656,#6654,#3984,.T.);
#8310=EDGE_CURVE('',#6655,#6657,#3985,.T.);
#8311=EDGE_CURVE('',#6657,#6658,#3986,.T.);
#8312=EDGE_CURVE('',#6658,#6656,#3987,.T.);
#8313=EDGE_CURVE('',#6657,#6659,#3988,.T.);
#8314=EDGE_CURVE('',#6659,#6660,#3989,.T.);
#8315=EDGE_CURVE('',#6660,#6658,#3990,.T.);
#8316=EDGE_CURVE('',#6659,#6649,#3991,.T.);
#8317=EDGE_CURVE('',#6652,#6660,#3992,.T.);
#11566=ORIENTED_EDGE('',*,*,#8286,.F.);
#11567=ORIENTED_EDGE('',*,*,#8287,.F.);
#11568=ORIENTED_EDGE('',*,*,#8288,.T.);
#11569=ORIENTED_EDGE('',*,*,#8286,.T.);
#11570=ORIENTED_EDGE('',*,*,#8288,.F.);
#11571=ORIENTED_EDGE('',*,*,#8289,.F.);
#11572=ORIENTED_EDGE('',*,*,#8290,.T.);
#11573=ORIENTED_EDGE('',*,*,#8287,.T.);
#11574=ORIENTED_EDGE('',*,*,#8290,.F.);
#11575=ORIENTED_EDGE('',*,*,#8291,.F.);
#11576=ORIENTED_EDGE('',*,*,#8292,.T.);
#11577=ORIENTED_EDGE('',*,*,#8289,.T.);
#11578=ORIENTED_EDGE('',*,*,#8292,.F.);
#11579=ORIENTED_EDGE('',*,*,#8291,.T.);
#11580=ORIENTED_EDGE('',*,*,#8293,.F.);
#11581=ORIENTED_EDGE('',*,*,#8294,.F.);
#11582=ORIENTED_EDGE('',*,*,#8295,.T.);
#11583=ORIENTED_EDGE('',*,*,#8293,.T.);
#11584=ORIENTED_EDGE('',*,*,#8295,.F.);
#11585=ORIENTED_EDGE('',*,*,#8296,.F.);
#11586=ORIENTED_EDGE('',*,*,#8297,.T.);
#11587=ORIENTED_EDGE('',*,*,#8294,.T.);
#11588=ORIENTED_EDGE('',*,*,#8297,.F.);
#11589=ORIENTED_EDGE('',*,*,#8298,.F.);
#11590=ORIENTED_EDGE('',*,*,#8299,.T.);
#11591=ORIENTED_EDGE('',*,*,#8296,.T.);
#11592=ORIENTED_EDGE('',*,*,#8299,.F.);
#11593=ORIENTED_EDGE('',*,*,#8298,.T.);
#11594=ORIENTED_EDGE('',*,*,#8300,.T.);
#11595=ORIENTED_EDGE('',*,*,#8301,.T.);
#11596=ORIENTED_EDGE('',*,*,#8302,.T.);
#11597=ORIENTED_EDGE('',*,*,#8303,.F.);
#11598=ORIENTED_EDGE('',*,*,#8304,.T.);
#11599=ORIENTED_EDGE('',*,*,#8305,.T.);
#11600=ORIENTED_EDGE('',*,*,#8306,.T.);
#11601=ORIENTED_EDGE('',*,*,#8301,.F.);
#11602=ORIENTED_EDGE('',*,*,#8307,.T.);
#11603=ORIENTED_EDGE('',*,*,#8308,.T.);
#11604=ORIENTED_EDGE('',*,*,#8309,.T.);
#11605=ORIENTED_EDGE('',*,*,#8305,.F.);
#11606=ORIENTED_EDGE('',*,*,#8310,.T.);
#11607=ORIENTED_EDGE('',*,*,#8311,.T.);
#11608=ORIENTED_EDGE('',*,*,#8312,.T.);
#11609=ORIENTED_EDGE('',*,*,#8308,.F.);
#11610=ORIENTED_EDGE('',*,*,#8313,.T.);
#11611=ORIENTED_EDGE('',*,*,#8314,.T.);
#11612=ORIENTED_EDGE('',*,*,#8315,.T.);
#11613=ORIENTED_EDGE('',*,*,#8311,.F.);
#11614=ORIENTED_EDGE('',*,*,#8316,.T.);
#11615=ORIENTED_EDGE('',*,*,#8303,.T.);
#11616=ORIENTED_EDGE('',*,*,#8317,.T.);
#11617=ORIENTED_EDGE('',*,*,#8314,.F.);
#11618=ORIENTED_EDGE('',*,*,#8316,.F.);
#11619=ORIENTED_EDGE('',*,*,#8313,.F.);
#11620=ORIENTED_EDGE('',*,*,#8310,.F.);
#11621=ORIENTED_EDGE('',*,*,#8307,.F.);
#11622=ORIENTED_EDGE('',*,*,#8304,.F.);
#11623=ORIENTED_EDGE('',*,*,#8300,.F.);
#11624=ORIENTED_EDGE('',*,*,#8317,.F.);
#11625=ORIENTED_EDGE('',*,*,#8302,.F.);
#11626=ORIENTED_EDGE('',*,*,#8306,.F.);
#11627=ORIENTED_EDGE('',*,*,#8309,.F.);
#11628=ORIENTED_EDGE('',*,*,#8312,.F.);
#11629=ORIENTED_EDGE('',*,*,#8315,.F.);
#11798=CYLINDRICAL_SURFACE('',#14056,0.35);
#11799=CYLINDRICAL_SURFACE('',#14064,0.1954);
#12462=ADVANCED_FACE('',(#1953),#1280,.T.);
#12463=ADVANCED_FACE('',(#1954),#494,.T.);
#12464=ADVANCED_FACE('',(#1955),#11798,.T.);
#12465=ADVANCED_FACE('',(#1956),#495,.T.);
#12466=ADVANCED_FACE('',(#1957,#846),#1281,.T.);
#12467=ADVANCED_FACE('',(#1958),#496,.T.);
#12468=ADVANCED_FACE('',(#1959),#11799,.T.);
#12469=ADVANCED_FACE('',(#1960),#497,.T.);
#12470=ADVANCED_FACE('',(#1961),#1282,.T.);
#12471=ADVANCED_FACE('',(#1962),#1283,.F.);
#12472=ADVANCED_FACE('',(#1963),#1284,.F.);
#12473=ADVANCED_FACE('',(#1964),#1285,.F.);
#12474=ADVANCED_FACE('',(#1965),#1286,.F.);
#12475=ADVANCED_FACE('',(#1966),#1287,.F.);
#12476=ADVANCED_FACE('',(#1967),#1288,.F.);
#12477=ADVANCED_FACE('',(#1968),#1289,.F.);
#12478=ADVANCED_FACE('',(#1969),#1290,.F.);
#12533=CLOSED_SHELL('',(#12462,#12463,#12464,#12465,#12466,#12467,#12468,
#12469,#12470));
#12534=CLOSED_SHELL('',(#12471,#12472,#12473,#12474,#12475,#12476,#12477,
#12478));
#14051=AXIS2_PLACEMENT_3D('',#32500,#17404,#17405);
#14052=AXIS2_PLACEMENT_3D('',#32501,#17406,#17407);
#14053=AXIS2_PLACEMENT_3D('',#32503,#17408,#17409);
#14054=AXIS2_PLACEMENT_3D('',#32504,#17410,#17411);
#14055=AXIS2_PLACEMENT_3D('',#32506,#17412,#17413);
#14056=AXIS2_PLACEMENT_3D('',#32508,#17415,#17416);
#14057=AXIS2_PLACEMENT_3D('',#32510,#17417,#17418);
#14058=AXIS2_PLACEMENT_3D('',#32512,#17420,#17421);
#14059=AXIS2_PLACEMENT_3D('',#32514,#17422,#17423);
#14060=AXIS2_PLACEMENT_3D('',#32516,#17425,#17426);
#14061=AXIS2_PLACEMENT_3D('',#32518,#17427,#17428);
#14062=AXIS2_PLACEMENT_3D('',#32519,#17429,#17430);
#14063=AXIS2_PLACEMENT_3D('',#32521,#17431,#17432);
#14064=AXIS2_PLACEMENT_3D('',#32523,#17434,#17435);
#14065=AXIS2_PLACEMENT_3D('',#32525,#17436,#17437);
#14066=AXIS2_PLACEMENT_3D('',#32527,#17439,#17440);
#14067=AXIS2_PLACEMENT_3D('',#32529,#17441,#17442);
#14068=AXIS2_PLACEMENT_3D('',#32531,#17444,#17445);
#14069=AXIS2_PLACEMENT_3D('',#32532,#17446,#17447);
#14070=AXIS2_PLACEMENT_3D('',#32541,#17452,#17453);
#14071=AXIS2_PLACEMENT_3D('',#32547,#17457,#17458);
#14072=AXIS2_PLACEMENT_3D('',#32553,#17462,#17463);
#14073=AXIS2_PLACEMENT_3D('',#32559,#17467,#17468);
#14074=AXIS2_PLACEMENT_3D('',#32565,#17472,#17473);
#14075=AXIS2_PLACEMENT_3D('',#32568,#17476,#17477);
#14076=AXIS2_PLACEMENT_3D('',#32569,#17478,#17479);
#17404=DIRECTION('axis',(0.,0.,1.));
#17405=DIRECTION('refdir',(1.,0.,0.));
#17406=DIRECTION('center_axis',(0.,1.,0.));
#17407=DIRECTION('ref_axis',(0.,0.,1.));
#17408=DIRECTION('center_axis',(0.,-1.,0.));
#17409=DIRECTION('ref_axis',(1.,0.,0.));
#17410=DIRECTION('center_axis',(0.,-1.,0.));
#17411=DIRECTION('ref_axis',(1.,0.,0.));
#17412=DIRECTION('center_axis',(0.,-1.,0.));
#17413=DIRECTION('ref_axis',(1.,0.,0.));
#17414=DIRECTION('',(0.707106781186547,0.707106781186548,8.65956056235493E-17));
#17415=DIRECTION('center_axis',(0.,-1.,0.));
#17416=DIRECTION('ref_axis',(1.,0.,0.));
#17417=DIRECTION('center_axis',(0.,-1.,0.));
#17418=DIRECTION('ref_axis',(1.,0.,0.));
#17419=DIRECTION('',(0.,1.,0.));
#17420=DIRECTION('center_axis',(0.,1.,0.));
#17421=DIRECTION('ref_axis',(1.,0.,0.));
#17422=DIRECTION('center_axis',(0.,-1.,0.));
#17423=DIRECTION('ref_axis',(1.,0.,0.));
#17424=DIRECTION('',(-0.707106781186547,0.707106781186548,-8.65956056235493E-17));
#17425=DIRECTION('center_axis',(0.,-1.,0.));
#17426=DIRECTION('ref_axis',(0.,0.,-1.));
#17427=DIRECTION('center_axis',(0.,-1.,0.));
#17428=DIRECTION('ref_axis',(1.,0.,0.));
#17429=DIRECTION('center_axis',(0.,1.,0.));
#17430=DIRECTION('ref_axis',(1.,0.,0.));
#17431=DIRECTION('center_axis',(0.,1.,0.));
#17432=DIRECTION('ref_axis',(1.,0.,0.));
#17433=DIRECTION('',(-0.447213595499958,0.894427190999916,-5.47678698264203E-17));
#17434=DIRECTION('center_axis',(0.,-1.,0.));
#17435=DIRECTION('ref_axis',(1.,0.,0.));
#17436=DIRECTION('center_axis',(0.,1.,0.));
#17437=DIRECTION('ref_axis',(1.,0.,0.));
#17438=DIRECTION('',(0.,1.,0.));
#17439=DIRECTION('center_axis',(0.,1.,0.));
#17440=DIRECTION('ref_axis',(1.,0.,0.));
#17441=DIRECTION('center_axis',(0.,-1.,0.));
#17442=DIRECTION('ref_axis',(1.,0.,0.));
#17443=DIRECTION('',(-0.707106781186547,0.707106781186548,-8.65956056235493E-17));
#17444=DIRECTION('center_axis',(0.,-1.,0.));
#17445=DIRECTION('ref_axis',(0.,0.,-1.));
#17446=DIRECTION('center_axis',(0.866025403784439,0.,-0.5));
#17447=DIRECTION('ref_axis',(0.5,0.,0.866025403784439));
#17448=DIRECTION('',(-0.5,0.,-0.866025403784439));
#17449=DIRECTION('',(0.,-1.,0.));
#17450=DIRECTION('',(0.5,0.,0.866025403784439));
#17451=DIRECTION('',(0.,-1.,0.));
#17452=DIRECTION('center_axis',(1.60246890531964E-16,0.,-1.));
#17453=DIRECTION('ref_axis',(1.,0.,1.60246890531964E-16));
#17454=DIRECTION('',(-1.,0.,-1.60246890531964E-16));
#17455=DIRECTION('',(0.,-1.,0.));
#17456=DIRECTION('',(1.,0.,1.60246890531964E-16));
#17457=DIRECTION('center_axis',(-0.866025403784439,0.,-0.5));
#17458=DIRECTION('ref_axis',(0.5,0.,-0.866025403784439));
#17459=DIRECTION('',(-0.5,0.,0.866025403784439));
#17460=DIRECTION('',(0.,-1.,0.));
#17461=DIRECTION('',(0.5,0.,-0.866025403784439));
#17462=DIRECTION('center_axis',(-0.866025403784439,0.,0.5));
#17463=DIRECTION('ref_axis',(-0.5,0.,-0.866025403784439));
#17464=DIRECTION('',(0.5,0.,0.866025403784439));
#17465=DIRECTION('',(0.,-1.,0.));
#17466=DIRECTION('',(-0.5,0.,-0.866025403784439));
#17467=DIRECTION('center_axis',(-1.60246890531964E-16,0.,1.));
#17468=DIRECTION('ref_axis',(-1.,0.,-1.60246890531964E-16));
#17469=DIRECTION('',(1.,0.,1.60246890531964E-16));
#17470=DIRECTION('',(0.,-1.,0.));
#17471=DIRECTION('',(-1.,0.,-1.60246890531964E-16));
#17472=DIRECTION('center_axis',(0.866025403784439,0.,0.5));
#17473=DIRECTION('ref_axis',(-0.5,0.,0.866025403784439));
#17474=DIRECTION('',(0.5,0.,-0.866025403784439));
#17475=DIRECTION('',(-0.5,0.,0.866025403784439));
#17476=DIRECTION('center_axis',(0.,1.,0.));
#17477=DIRECTION('ref_axis',(1.,0.,0.));
#17478=DIRECTION('center_axis',(0.,-1.,0.));
#17479=DIRECTION('ref_axis',(0.,0.,-1.));
#32500=CARTESIAN_POINT('',(0.,0.,0.));
#32501=CARTESIAN_POINT('Origin',(0.3,0.4,0.));
#32502=CARTESIAN_POINT('',(-0.3,0.4,-3.67394039744206E-17));
#32503=CARTESIAN_POINT('Origin',(0.,0.4,0.));
#32504=CARTESIAN_POINT('Origin',(0.,0.375,0.));
#32505=CARTESIAN_POINT('',(-0.35,0.35,-4.28626379701573E-17));
#32506=CARTESIAN_POINT('Origin',(0.,0.35,0.));
#32507=CARTESIAN_POINT('',(-0.325,0.375,-3.9801020972289E-17));
#32508=CARTESIAN_POINT('Origin',(0.,0.19,0.));
#32509=CARTESIAN_POINT('',(-0.35,0.03,-4.28626379701574E-17));
#32510=CARTESIAN_POINT('Origin',(0.,0.03,0.));
#32511=CARTESIAN_POINT('',(-0.35,0.19,-4.28626379701574E-17));
#32512=CARTESIAN_POINT('Origin',(0.,0.0149999999999999,0.));
#32513=CARTESIAN_POINT('',(-0.32,-3.29597460435593E-17,-3.91886975727153E-17));
#32514=CARTESIAN_POINT('Origin',(0.,0.,0.));
#32515=CARTESIAN_POINT('',(-0.335,0.0149999999999999,-4.10256677714363E-17));
#32516=CARTESIAN_POINT('Origin',(0.22,0.,0.));
#32517=CARTESIAN_POINT('',(-0.22,-6.93889390390723E-18,-2.69422295812418E-17));
#32518=CARTESIAN_POINT('Origin',(0.,0.,0.));
#32519=CARTESIAN_POINT('Origin',(0.,-0.02,0.));
#32520=CARTESIAN_POINT('',(-0.1954,-0.0492,2.39295984553393E-17));
#32521=CARTESIAN_POINT('Origin',(0.,-0.0492,0.));
#32522=CARTESIAN_POINT('',(-0.21,-0.02,-2.57175827820944E-17));
#32523=CARTESIAN_POINT('Origin',(0.,-0.8,0.));
#32524=CARTESIAN_POINT('',(-0.1954,-1.5646,2.39295984553393E-17));
#32525=CARTESIAN_POINT('Origin',(0.,-1.5646,0.));
#32526=CARTESIAN_POINT('',(-0.1954,-0.8,-2.39295984553393E-17));
#32527=CARTESIAN_POINT('Origin',(0.,-1.58,0.));
#32528=CARTESIAN_POINT('',(-0.16,-1.6,-1.95943487863577E-17));
#32529=CARTESIAN_POINT('Origin',(0.,-1.6,0.));
#32530=CARTESIAN_POINT('',(-0.18,-1.58,-2.20436423846524E-17));
#32531=CARTESIAN_POINT('Origin',(0.,-1.6,0.));
#32532=CARTESIAN_POINT('Origin',(0.0866025403784439,-0.4,-0.15));
#32533=CARTESIAN_POINT('',(0.173205080756888,-0.4,0.));
#32534=CARTESIAN_POINT('',(0.0866025403784439,-0.4,-0.15));
#32535=CARTESIAN_POINT('',(0.173205080756888,-0.4,0.));
#32536=CARTESIAN_POINT('',(0.0866025403784439,-0.64,-0.15));
#32537=CARTESIAN_POINT('',(0.0866025403784439,-0.4,-0.15));
#32538=CARTESIAN_POINT('',(0.173205080756888,-0.64,0.));
#32539=CARTESIAN_POINT('',(0.173205080756888,-0.64,0.));
#32540=CARTESIAN_POINT('',(0.173205080756888,-0.4,0.));
#32541=CARTESIAN_POINT('Origin',(-0.0866025403784438,-0.4,-0.15));
#32542=CARTESIAN_POINT('',(-0.0866025403784438,-0.4,-0.15));
#32543=CARTESIAN_POINT('',(0.0866025403784439,-0.4,-0.15));
#32544=CARTESIAN_POINT('',(-0.0866025403784438,-0.64,-0.15));
#32545=CARTESIAN_POINT('',(-0.0866025403784438,-0.4,-0.15));
#32546=CARTESIAN_POINT('',(0.0866025403784439,-0.64,-0.15));
#32547=CARTESIAN_POINT('Origin',(-0.173205080756888,-0.4,-2.77555756156289E-17));
#32548=CARTESIAN_POINT('',(-0.173205080756888,-0.4,-2.12115047744981E-17));
#32549=CARTESIAN_POINT('',(-0.0866025403784438,-0.4,-0.15));
#32550=CARTESIAN_POINT('',(-0.173205080756888,-0.64,-2.77555756156289E-17));
#32551=CARTESIAN_POINT('',(-0.173205080756888,-0.4,-2.12115047744981E-17));
#32552=CARTESIAN_POINT('',(-0.0866025403784438,-0.64,-0.15));
#32553=CARTESIAN_POINT('Origin',(-0.0866025403784439,-0.4,0.15));
#32554=CARTESIAN_POINT('',(-0.0866025403784439,-0.4,0.15));
#32555=CARTESIAN_POINT('',(-0.173205080756888,-0.4,-2.12115047744981E-17));
#32556=CARTESIAN_POINT('',(-0.0866025403784439,-0.64,0.15));
#32557=CARTESIAN_POINT('',(-0.0866025403784439,-0.4,0.15));
#32558=CARTESIAN_POINT('',(-0.173205080756888,-0.64,-2.12115047744981E-17));
#32559=CARTESIAN_POINT('Origin',(0.0866025403784439,-0.4,0.15));
#32560=CARTESIAN_POINT('',(0.0866025403784439,-0.4,0.15));
#32561=CARTESIAN_POINT('',(-0.0866025403784439,-0.4,0.15));
#32562=CARTESIAN_POINT('',(0.0866025403784439,-0.64,0.15));
#32563=CARTESIAN_POINT('',(0.0866025403784439,-0.4,0.15));
#32564=CARTESIAN_POINT('',(-0.0866025403784439,-0.64,0.15));
#32565=CARTESIAN_POINT('Origin',(0.173205080756888,-0.4,0.));
#32566=CARTESIAN_POINT('',(0.0866025403784439,-0.4,0.15));
#32567=CARTESIAN_POINT('',(0.0866025403784439,-0.64,0.15));
#32568=CARTESIAN_POINT('Origin',(0.,-0.4,-2.77555756156289E-17));
#32569=CARTESIAN_POINT('Origin',(0.,-0.64,-2.77555756156289E-17));
#32699=UNCERTAINTY_MEASURE_WITH_UNIT(LENGTH_MEASURE(0.001),#32752,
'DISTANCE_ACCURACY_VALUE',
'Maximum model space distance between geometric entities at asserted c
onnectivities');
#32702=UNCERTAINTY_MEASURE_WITH_UNIT(LENGTH_MEASURE(0.001),#32752,
'DISTANCE_ACCURACY_VALUE',
'Maximum model space distance between geometric entities at asserted c
onnectivities');
#32748=(
GEOMETRIC_REPRESENTATION_CONTEXT(3)
GLOBAL_UNCERTAINTY_ASSIGNED_CONTEXT((#32699))
GLOBAL_UNIT_ASSIGNED_CONTEXT((#32752,#32754,#32755))
REPRESENTATION_CONTEXT('','3D')
);
#32751=(
GEOMETRIC_REPRESENTATION_CONTEXT(3)
GLOBAL_UNCERTAINTY_ASSIGNED_CONTEXT((#32702))
GLOBAL_UNIT_ASSIGNED_CONTEXT((#32752,#32754,#32755))
REPRESENTATION_CONTEXT('','3D')
);
#32752=(
LENGTH_UNIT()
NAMED_UNIT(*)
SI_UNIT(.CENTI.,.METRE.)
);
#32754=(
NAMED_UNIT(*)
PLANE_ANGLE_UNIT()
SI_UNIT($,.RADIAN.)
);
#32755=(
NAMED_UNIT(*)
SI_UNIT($,.STERADIAN.)
SOLID_ANGLE_UNIT()
);
#32801=SHAPE_DEFINITION_REPRESENTATION(#32858,#32974);
#32858=PRODUCT_DEFINITION_SHAPE('',$,#33023);
#32974=SHAPE_REPRESENTATION('',(#14051),#32748);
#32977=PRODUCT_DEFINITION_CONTEXT('part definition',#33123,'design');
#33023=PRODUCT_DEFINITION('Cap Screw - M4x16','Cap Screw - M4x16',#33071,
#32977);
#33071=PRODUCT_DEFINITION_FORMATION('',$,#33170);
#33123=APPLICATION_CONTEXT(
'Core Data for Automotive Mechanical Design Process');
#33124=PRODUCT_CONTEXT('part definition',#33123,'mechanical');
#33170=PRODUCT('Cap Screw - M4x16','Cap Screw - M4x16',
'Cap Screw - M4x16',(#33124));
#33243=COLOUR_RGB('Black',0.12,0.14,0.17);
#33244=FILL_AREA_STYLE_COLOUR('',#33243);
#33245=FILL_AREA_STYLE('',(#33244));
#33246=SURFACE_STYLE_FILL_AREA(#33245);
#33247=SURFACE_SIDE_STYLE('',(#33246));
#33248=SURFACE_STYLE_USAGE(.BOTH.,#33247);
#33249=PRESENTATION_STYLE_ASSIGNMENT((#33248));
ENDSEC;
END-ISO-10303-21;
